ISO-10303-21;
HEADER;
/* Generated by software containing ST-Developer
 * from STEP Tools, Inc. (www.steptools.com) 
 */

FILE_DESCRIPTION(
/* description */ (''),
/* implementation_level */ '2;1');

FILE_NAME(
/* name */ 'Base.step',
/* time_stamp */ '2026-09-20T21:58:27+06:00',
/* author */ (''),
/* organization */ (''),
/* preprocessor_version */ 'ST-DEVELOPER v20.2',
/* originating_system */ 'Autodesk Translation Framework v15.15.0.0',
/* authorisation */ '');

FILE_SCHEMA (('AUTOMOTIVE_DESIGN { 1 0 10303 214 3 1 1 }'));
ENDSEC;

DATA;
#10=MECHANICAL_DESIGN_GEOMETRIC_PRESENTATION_REPRESENTATION('',(#66),#2238);
#50=SHAPE_REPRESENTATION_RELATIONSHIP('SRR','None',#2277,#58);
#58=ADVANCED_BREP_SHAPE_REPRESENTATION('',(#74),#2237);
#66=STYLED_ITEM('',(#2321),#74);
#74=MANIFOLD_SOLID_BREP('Base',#1213);
#85=FACE_BOUND('',#264,.T.);
#86=FACE_BOUND('',#265,.T.);
#87=FACE_BOUND('',#271,.T.);
#88=FACE_BOUND('',#272,.T.);
#115=PLANE('',#1449);
#116=PLANE('',#1450);
#117=PLANE('',#1451);
#118=PLANE('',#1452);
#119=PLANE('',#1453);
#120=PLANE('',#1454);
#182=FACE_OUTER_BOUND('',#261,.T.);
#183=FACE_OUTER_BOUND('',#262,.T.);
#184=FACE_OUTER_BOUND('',#263,.T.);
#185=FACE_OUTER_BOUND('',#266,.T.);
#186=FACE_OUTER_BOUND('',#267,.T.);
#187=FACE_OUTER_BOUND('',#268,.T.);
#188=FACE_OUTER_BOUND('',#269,.T.);
#189=FACE_OUTER_BOUND('',#270,.T.);
#261=EDGE_LOOP('',(#1064,#1065,#1066,#1067));
#262=EDGE_LOOP('',(#1068,#1069,#1070,#1071));
#263=EDGE_LOOP('',(#1072,#1073,#1074,#1075));
#264=EDGE_LOOP('',(#1076));
#265=EDGE_LOOP('',(#1077));
#266=EDGE_LOOP('',(#1078,#1079,#1080,#1081));
#267=EDGE_LOOP('',(#1082,#1083,#1084,#1085));
#268=EDGE_LOOP('',(#1086,#1087,#1088,#1089));
#269=EDGE_LOOP('',(#1090,#1091,#1092,#1093));
#270=EDGE_LOOP('',(#1094,#1095,#1096,#1097));
#271=EDGE_LOOP('',(#1098));
#272=EDGE_LOOP('',(#1099));
#344=LINE('',#2177,#429);
#345=LINE('',#2183,#430);
#346=LINE('',#2188,#431);
#347=LINE('',#2190,#432);
#348=LINE('',#2192,#433);
#349=LINE('',#2193,#434);
#350=LINE('',#2196,#435);
#351=LINE('',#2198,#436);
#352=LINE('',#2199,#437);
#353=LINE('',#2202,#438);
#354=LINE('',#2203,#439);
#355=LINE('',#2206,#440);
#356=LINE('',#2207,#441);
#357=LINE('',#2209,#442);
#429=VECTOR('',#1818,2.5);
#430=VECTOR('',#1825,2.5);
#431=VECTOR('',#1830,10.);
#432=VECTOR('',#1831,10.);
#433=VECTOR('',#1832,10.);
#434=VECTOR('',#1833,10.);
#435=VECTOR('',#1836,10.);
#436=VECTOR('',#1837,10.);
#437=VECTOR('',#1838,10.);
#438=VECTOR('',#1841,10.);
#439=VECTOR('',#1842,10.);
#440=VECTOR('',#1845,10.);
#441=VECTOR('',#1846,10.);
#442=VECTOR('',#1849,10.);
#513=CIRCLE('',#1444,2.5);
#514=CIRCLE('',#1445,2.5);
#515=CIRCLE('',#1447,2.5);
#516=CIRCLE('',#1448,2.5);
#611=VERTEX_POINT('',#2174);
#612=VERTEX_POINT('',#2176);
#613=VERTEX_POINT('',#2180);
#614=VERTEX_POINT('',#2182);
#615=VERTEX_POINT('',#2186);
#616=VERTEX_POINT('',#2187);
#617=VERTEX_POINT('',#2189);
#618=VERTEX_POINT('',#2191);
#619=VERTEX_POINT('',#2195);
#620=VERTEX_POINT('',#2197);
#621=VERTEX_POINT('',#2201);
#622=VERTEX_POINT('',#2205);
#764=EDGE_CURVE('',#611,#611,#513,.T.);
#765=EDGE_CURVE('',#611,#612,#344,.T.);
#766=EDGE_CURVE('',#612,#612,#514,.T.);
#767=EDGE_CURVE('',#613,#613,#515,.T.);
#768=EDGE_CURVE('',#613,#614,#345,.T.);
#769=EDGE_CURVE('',#614,#614,#516,.T.);
#770=EDGE_CURVE('',#615,#616,#346,.T.);
#771=EDGE_CURVE('',#617,#615,#347,.T.);
#772=EDGE_CURVE('',#618,#617,#348,.T.);
#773=EDGE_CURVE('',#616,#618,#349,.T.);
#774=EDGE_CURVE('',#615,#619,#350,.T.);
#775=EDGE_CURVE('',#620,#619,#351,.T.);
#776=EDGE_CURVE('',#617,#620,#352,.T.);
#777=EDGE_CURVE('',#616,#621,#353,.T.);
#778=EDGE_CURVE('',#619,#621,#354,.T.);
#779=EDGE_CURVE('',#622,#620,#355,.T.);
#780=EDGE_CURVE('',#618,#622,#356,.T.);
#781=EDGE_CURVE('',#621,#622,#357,.T.);
#1064=ORIENTED_EDGE('',*,*,#764,.F.);
#1065=ORIENTED_EDGE('',*,*,#765,.T.);
#1066=ORIENTED_EDGE('',*,*,#766,.F.);
#1067=ORIENTED_EDGE('',*,*,#765,.F.);
#1068=ORIENTED_EDGE('',*,*,#767,.F.);
#1069=ORIENTED_EDGE('',*,*,#768,.T.);
#1070=ORIENTED_EDGE('',*,*,#769,.T.);
#1071=ORIENTED_EDGE('',*,*,#768,.F.);
#1072=ORIENTED_EDGE('',*,*,#770,.F.);
#1073=ORIENTED_EDGE('',*,*,#771,.F.);
#1074=ORIENTED_EDGE('',*,*,#772,.F.);
#1075=ORIENTED_EDGE('',*,*,#773,.F.);
#1076=ORIENTED_EDGE('',*,*,#769,.F.);
#1077=ORIENTED_EDGE('',*,*,#766,.T.);
#1078=ORIENTED_EDGE('',*,*,#771,.T.);
#1079=ORIENTED_EDGE('',*,*,#774,.T.);
#1080=ORIENTED_EDGE('',*,*,#775,.F.);
#1081=ORIENTED_EDGE('',*,*,#776,.F.);
#1082=ORIENTED_EDGE('',*,*,#770,.T.);
#1083=ORIENTED_EDGE('',*,*,#777,.T.);
#1084=ORIENTED_EDGE('',*,*,#778,.F.);
#1085=ORIENTED_EDGE('',*,*,#774,.F.);
#1086=ORIENTED_EDGE('',*,*,#772,.T.);
#1087=ORIENTED_EDGE('',*,*,#776,.T.);
#1088=ORIENTED_EDGE('',*,*,#779,.F.);
#1089=ORIENTED_EDGE('',*,*,#780,.F.);
#1090=ORIENTED_EDGE('',*,*,#773,.T.);
#1091=ORIENTED_EDGE('',*,*,#780,.T.);
#1092=ORIENTED_EDGE('',*,*,#781,.F.);
#1093=ORIENTED_EDGE('',*,*,#777,.F.);
#1094=ORIENTED_EDGE('',*,*,#778,.T.);
#1095=ORIENTED_EDGE('',*,*,#781,.T.);
#1096=ORIENTED_EDGE('',*,*,#779,.T.);
#1097=ORIENTED_EDGE('',*,*,#775,.T.);
#1098=ORIENTED_EDGE('',*,*,#764,.T.);
#1099=ORIENTED_EDGE('',*,*,#767,.T.);
#1135=CYLINDRICAL_SURFACE('',#1443,2.5);
#1136=CYLINDRICAL_SURFACE('',#1446,2.5);
#1198=ADVANCED_FACE('',(#182),#1135,.F.);
#1199=ADVANCED_FACE('',(#183),#1136,.F.);
#1200=ADVANCED_FACE('',(#184,#85,#86),#115,.F.);
#1201=ADVANCED_FACE('',(#185),#116,.T.);
#1202=ADVANCED_FACE('',(#186),#117,.T.);
#1203=ADVANCED_FACE('',(#187),#118,.T.);
#1204=ADVANCED_FACE('',(#188),#119,.T.);
#1205=ADVANCED_FACE('',(#189,#87,#88),#120,.T.);
#1213=CLOSED_SHELL('',(#1198,#1199,#1200,#1201,#1202,#1203,#1204,#1205));
#1442=AXIS2_PLACEMENT_3D('',#2172,#1812,#1813);
#1443=AXIS2_PLACEMENT_3D('',#2173,#1814,#1815);
#1444=AXIS2_PLACEMENT_3D('',#2175,#1816,#1817);
#1445=AXIS2_PLACEMENT_3D('',#2178,#1819,#1820);
#1446=AXIS2_PLACEMENT_3D('',#2179,#1821,#1822);
#1447=AXIS2_PLACEMENT_3D('',#2181,#1823,#1824);
#1448=AXIS2_PLACEMENT_3D('',#2184,#1826,#1827);
#1449=AXIS2_PLACEMENT_3D('',#2185,#1828,#1829);
#1450=AXIS2_PLACEMENT_3D('',#2194,#1834,#1835);
#1451=AXIS2_PLACEMENT_3D('',#2200,#1839,#1840);
#1452=AXIS2_PLACEMENT_3D('',#2204,#1843,#1844);
#1453=AXIS2_PLACEMENT_3D('',#2208,#1847,#1848);
#1454=AXIS2_PLACEMENT_3D('',#2210,#1850,#1851);
#1812=DIRECTION('axis',(0.,0.,1.));
#1813=DIRECTION('refdir',(1.,0.,0.));
#1814=DIRECTION('center_axis',(0.,-1.,0.));
#1815=DIRECTION('ref_axis',(1.,0.,0.));
#1816=DIRECTION('center_axis',(0.,-1.,0.));
#1817=DIRECTION('ref_axis',(1.,0.,0.));
#1818=DIRECTION('',(0.,-1.,0.));
#1819=DIRECTION('center_axis',(0.,1.,0.));
#1820=DIRECTION('ref_axis',(1.,0.,0.));
#1821=DIRECTION('center_axis',(0.,-1.,0.));
#1822=DIRECTION('ref_axis',(1.,0.,0.));
#1823=DIRECTION('center_axis',(0.,-1.,0.));
#1824=DIRECTION('ref_axis',(1.,0.,0.));
#1825=DIRECTION('',(0.,-1.,0.));
#1826=DIRECTION('center_axis',(0.,-1.,0.));
#1827=DIRECTION('ref_axis',(1.,0.,0.));
#1828=DIRECTION('center_axis',(0.,1.,0.));
#1829=DIRECTION('ref_axis',(0.,0.,1.));
#1830=DIRECTION('',(-1.,0.,0.));
#1831=DIRECTION('',(0.,0.,-1.));
#1832=DIRECTION('',(1.,0.,0.));
#1833=DIRECTION('',(0.,0.,1.));
#1834=DIRECTION('center_axis',(1.,0.,0.));
#1835=DIRECTION('ref_axis',(0.,0.,-1.));
#1836=DIRECTION('',(0.,1.,0.));
#1837=DIRECTION('',(0.,0.,-1.));
#1838=DIRECTION('',(0.,1.,0.));
#1839=DIRECTION('center_axis',(0.,0.,-1.));
#1840=DIRECTION('ref_axis',(-1.,0.,0.));
#1841=DIRECTION('',(0.,1.,0.));
#1842=DIRECTION('',(-1.,0.,0.));
#1843=DIRECTION('center_axis',(0.,0.,1.));
#1844=DIRECTION('ref_axis',(1.,0.,0.));
#1845=DIRECTION('',(1.,0.,0.));
#1846=DIRECTION('',(0.,1.,0.));
#1847=DIRECTION('center_axis',(-1.,0.,0.));
#1848=DIRECTION('ref_axis',(0.,0.,1.));
#1849=DIRECTION('',(0.,0.,1.));
#1850=DIRECTION('center_axis',(0.,1.,0.));
#1851=DIRECTION('ref_axis',(0.,0.,1.));
#2172=CARTESIAN_POINT('',(0.,0.,0.));
#2173=CARTESIAN_POINT('Origin',(0.,3.,24.1717785126239));
#2174=CARTESIAN_POINT('',(-2.5,5.,24.1717785126239));
#2175=CARTESIAN_POINT('Origin',(0.,5.,24.1717785126239));
#2176=CARTESIAN_POINT('',(-2.5,3.,24.1717785126239));
#2177=CARTESIAN_POINT('',(-2.5,3.,24.1717785126239));
#2178=CARTESIAN_POINT('Origin',(0.,3.,24.1717785126239));
#2179=CARTESIAN_POINT('Origin',(0.,3.,64.2867316297599));
#2180=CARTESIAN_POINT('',(-2.5,5.,64.2867316297599));
#2181=CARTESIAN_POINT('Origin',(0.,5.,64.2867316297599));
#2182=CARTESIAN_POINT('',(-2.5,3.,64.2867316297599));
#2183=CARTESIAN_POINT('',(-2.5,3.,64.2867316297599));
#2184=CARTESIAN_POINT('Origin',(0.,3.,64.2867316297599));
#2185=CARTESIAN_POINT('Origin',(0.,3.,50.));
#2186=CARTESIAN_POINT('',(39.8793542860875,3.,-5.));
#2187=CARTESIAN_POINT('',(-39.8793542860875,3.,-5.));
#2188=CARTESIAN_POINT('',(19.9396771430438,3.,-5.));
#2189=CARTESIAN_POINT('',(39.8793542860875,3.,105.));
#2190=CARTESIAN_POINT('',(39.8793542860875,3.,77.5));
#2191=CARTESIAN_POINT('',(-39.8793542860875,3.,105.));
#2192=CARTESIAN_POINT('',(-19.9396771430438,3.,105.));
#2193=CARTESIAN_POINT('',(-39.8793542860875,3.,22.5));
#2194=CARTESIAN_POINT('Origin',(39.8793542860875,0.,105.));
#2195=CARTESIAN_POINT('',(39.8793542860875,5.,-5.));
#2196=CARTESIAN_POINT('',(39.8793542860875,0.,-5.));
#2197=CARTESIAN_POINT('',(39.8793542860875,5.,105.));
#2198=CARTESIAN_POINT('',(39.8793542860875,5.,105.));
#2199=CARTESIAN_POINT('',(39.8793542860875,0.,105.));
#2200=CARTESIAN_POINT('Origin',(39.8793542860875,0.,-5.));
#2201=CARTESIAN_POINT('',(-39.8793542860875,5.,-5.));
#2202=CARTESIAN_POINT('',(-39.8793542860875,0.,-5.));
#2203=CARTESIAN_POINT('',(39.8793542860875,5.,-5.));
#2204=CARTESIAN_POINT('Origin',(-39.8793542860875,0.,105.));
#2205=CARTESIAN_POINT('',(-39.8793542860875,5.,105.));
#2206=CARTESIAN_POINT('',(-39.8793542860875,5.,105.));
#2207=CARTESIAN_POINT('',(-39.8793542860875,0.,105.));
#2208=CARTESIAN_POINT('Origin',(-39.8793542860875,0.,-5.));
#2209=CARTESIAN_POINT('',(-39.8793542860875,5.,-5.));
#2210=CARTESIAN_POINT('Origin',(0.,5.,50.));
#2227=UNCERTAINTY_MEASURE_WITH_UNIT(LENGTH_MEASURE(0.01),#2239,
'DISTANCE_ACCURACY_VALUE',
'Maximum model space distance between geometric entities at asserted c
onnectivities');
#2228=UNCERTAINTY_MEASURE_WITH_UNIT(LENGTH_MEASURE(0.01),#2239,
'DISTANCE_ACCURACY_VALUE',
'Maximum model space distance between geometric entities at asserted c
onnectivities');
#2237=(
GEOMETRIC_REPRESENTATION_CONTEXT(3)
GLOBAL_UNCERTAINTY_ASSIGNED_CONTEXT((#2227))
GLOBAL_UNIT_ASSIGNED_CONTEXT((#2239,#2241,#2242))
REPRESENTATION_CONTEXT('','3D')
);
#2238=(
GEOMETRIC_REPRESENTATION_CONTEXT(3)
GLOBAL_UNCERTAINTY_ASSIGNED_CONTEXT((#2228))
GLOBAL_UNIT_ASSIGNED_CONTEXT((#2239,#2241,#2242))
REPRESENTATION_CONTEXT('','3D')
);
#2239=(
LENGTH_UNIT()
NAMED_UNIT(*)
SI_UNIT(.MILLI.,.METRE.)
);
#2241=(
NAMED_UNIT(*)
PLANE_ANGLE_UNIT()
SI_UNIT($,.RADIAN.)
);
#2242=(
NAMED_UNIT(*)
SI_UNIT($,.STERADIAN.)
SOLID_ANGLE_UNIT()
);
#2251=SHAPE_DEFINITION_REPRESENTATION(#2260,#2277);
#2260=PRODUCT_DEFINITION_SHAPE('',$,#2287);
#2277=SHAPE_REPRESENTATION('',(#1442),#2237);
#2278=PRODUCT_DEFINITION_CONTEXT('part definition',#2307,'design');
#2287=PRODUCT_DEFINITION('Base','Base',#2296,#2278);
#2296=PRODUCT_DEFINITION_FORMATION('',$,#2317);
#2307=APPLICATION_CONTEXT(
'Core Data for Automotive Mechanical Design Process');
#2308=PRODUCT_CONTEXT('part definition',#2307,'mechanical');
#2317=PRODUCT('Base','Base',$,(#2308));
#2321=PRESENTATION_STYLE_ASSIGNMENT((#2325));
#2325=SURFACE_STYLE_USAGE(.BOTH.,#2329);
#2329=SURFACE_SIDE_STYLE('',(#2333));
#2333=SURFACE_STYLE_FILL_AREA(#2337);
#2337=FILL_AREA_STYLE('Surface - Matte',(#2341));
#2341=FILL_AREA_STYLE_COLOUR('Surface - Matte',#2345);
#2345=COLOUR_RGB('Surface - Matte', 0.31764706, 0.68627451, 0.89019608);
ENDSEC;
END-ISO-10303-21;
